ISO-10303-21;
HEADER;
FILE_DESCRIPTION (('STEP AP214'),
    '1' );
FILE_NAME ('needle roller bearing_nm_iso_ISO 3030 - 15C5060 - 26,SI,AC,26.step',
    '2026-10-24T07:08:27',
    ( '' ),
    ( '' ),
    'SwSTEP 2.0',
    'SolidWorks 2026',
    '' );
FILE_SCHEMA (( 'AUTOMOTIVE_DESIGN' ));
ENDSEC;

DATA;
#48=DIRECTION ( 'NONE',  ( 1.000000000000000000, 0.000000000000000000, 0.000000000000000000 ) ) ;
#49=DIRECTION ( 'NONE',  ( 0.000000000000000000, -1.000000000000000000, 0.000000000000000000 ) ) ;
#54=ORIENTED_EDGE ( 'NONE', *, *, #7702, .F. ) ;
#77=FACE_OUTER_BOUND ( 'NONE', #12932, .T. ) ;
#154=EDGE_CURVE ( 'NONE', #2490, #16785, #5575, .T. ) ;
#164=ADVANCED_FACE ( 'NONE', ( #7241 ), #1349, .F. ) ;
#179=VERTEX_POINT ( 'NONE', #8579 ) ;
#192=VERTEX_POINT ( 'NONE', #13063 ) ;
#200=CIRCLE ( 'NONE', #7785, 30.00000000000000711 ) ;
#222=ORIENTED_EDGE ( 'NONE', *, *, #3085, .T. ) ;
#238=ORIENTED_EDGE ( 'NONE', *, *, #16129, .T. ) ;
#244=AXIS2_PLACEMENT_3D ( 'NONE', #7174, #48, #4147 ) ;
#274=EDGE_CURVE ( 'NONE', #652, #912, #17441, .T. ) ;
#316=ORIENTED_EDGE ( 'NONE', *, *, #16930, .F. ) ;
#354=EDGE_LOOP ( 'NONE', ( #10863, #11832 ) ) ;
#374=AXIS2_PLACEMENT_3D ( 'NONE', #16083, #3127, #12944 ) ;
#388=CARTESIAN_POINT ( 'NONE',  ( -11.15000000000000391, 3.673940397442059967E-15, -30.00000000000000711 ) ) ;
#414=DIRECTION ( 'NONE',  ( -1.000000000000000000, -0.000000000000000000, -0.000000000000000000 ) ) ;
#423=DIRECTION ( 'NONE',  ( 0.000000000000000000, 0.000000000000000000, 1.000000000000000000 ) ) ;
#432=VERTEX_POINT ( 'NONE', #5315 ) ;
#433=LINE ( 'NONE', #1768, #16474 ) ;
#438=STYLED_ITEM ( 'NONE', ( #4638 ), #574 ) ;
#453=DIRECTION ( 'NONE',  ( 1.000000000000000000, 0.000000000000000000, 0.000000000000000000 ) ) ;
#493=AXIS2_PLACEMENT_3D ( 'NONE', #10909, #12621, #9669 ) ;
#497=EDGE_CURVE ( 'NONE', #9138, #1316, #3398, .T. ) ;
#507=EDGE_CURVE ( 'NONE', #3158, #1316, #8188, .T. ) ;
#511=CARTESIAN_POINT ( 'NONE',  ( 11.14999999999999680, 0.000000000000000000, 0.000000000000000000 ) ) ;
#527=CIRCLE ( 'NONE', #8139, 28.00000000000000355 ) ;
#560=VERTEX_POINT ( 'NONE', #17852 ) ;
#574=ADVANCED_BREP_SHAPE_REPRESENTATION ( '', ( #3243, #8017 ), #16563 ) ;
#652=VERTEX_POINT ( 'NONE', #4706 ) ;
#654=DIRECTION ( 'NONE',  ( 0.000000000000000000, 0.000000000000000000, -1.000000000000000000 ) ) ;
#749=CARTESIAN_POINT ( 'NONE',  ( -11.25000000000000355, 0.000000000000000000, -27.00000000000000355 ) ) ;
#795=LINE ( 'NONE', #18309, #10102 ) ;
#829=DIRECTION ( 'NONE',  ( 0.000000000000000000, 0.000000000000000000, -1.000000000000000000 ) ) ;
#848=ORIENTED_EDGE ( 'NONE', *, *, #17503, .T. ) ;
#857=CARTESIAN_POINT ( 'NONE',  ( -17.77999999999999758, 0.000000000000000000, 0.000000000000000000 ) ) ;
#863=CARTESIAN_POINT ( 'NONE',  ( -11.25000000000000355, 0.000000000000000000, 0.000000000000000000 ) ) ;
#905=DIRECTION ( 'NONE',  ( 0.000000000000000000, 0.000000000000000000, 1.000000000000000000 ) ) ;
#912=VERTEX_POINT ( 'NONE', #14328 ) ;
#1068=EDGE_LOOP ( 'NONE', ( #4777, #8665 ) ) ;
#1089=ORIENTED_EDGE ( 'NONE', *, *, #8610, .F. ) ;
#1106=CARTESIAN_POINT ( 'NONE',  ( -11.15000000000000391, 0.000000000000000000, 0.000000000000000000 ) ) ;
#1170=EDGE_CURVE ( 'NONE', #7123, #7186, #9632, .T. ) ;
#1179=CIRCLE ( 'NONE', #4510, 30.00000000000000711 ) ;
#1228=CYLINDRICAL_SURFACE ( 'NONE', #13927, 28.00000000000000355 ) ;
#1250=DIRECTION ( 'NONE',  ( 0.000000000000000000, 0.000000000000000000, 1.000000000000000000 ) ) ;
#1256=EDGE_LOOP ( 'NONE', ( #7920, #17878, #8134, #16176 ) ) ;
#1257=DIRECTION ( 'NONE',  ( 0.000000000000000000, 0.000000000000000000, 1.000000000000000000 ) ) ;
#1262=ORIENTED_EDGE ( 'NONE', *, *, #16911, .T. ) ;
#1270=ORIENTED_EDGE ( 'NONE', *, *, #15484, .F. ) ;
#1280=EDGE_CURVE ( 'NONE', #3817, #3158, #10552, .T. ) ;
#1316=VERTEX_POINT ( 'NONE', #749 ) ;
#1320=DIRECTION ( 'NONE',  ( 0.000000000000000000, 0.000000000000000000, -1.000000000000000000 ) ) ;
#1327=CLOSED_SHELL ( 'NONE', ( #17965, #164, #14690, #13540, #3071, #12220, #17855, #6904, #18585, #8315, #17345, #16285, #11966, #5922, #5029, #11411, #5542, #6343, #15976, #1623, #14717, #17295, #12308, #8944, #14474, #5704 ) ) ;
#1349=CYLINDRICAL_SURFACE ( 'NONE', #8605, 27.00000000000000355 ) ;
#1377=DIRECTION ( 'NONE',  ( 1.000000000000000000, 0.000000000000000000, 0.000000000000000000 ) ) ;
#1449=EDGE_LOOP ( 'NONE', ( #12624, #5261 ) ) ;
#1486=VERTEX_POINT ( 'NONE', #13184 ) ;
#1511=( NAMED_UNIT ( * ) PLANE_ANGLE_UNIT ( ) SI_UNIT ( $, .RADIAN. ) );
#1515=AXIS2_PLACEMENT_3D ( 'NONE', #7052, #14200, #1257 ) ;
#1533=CIRCLE ( 'NONE', #16133, 27.00000000000000355 ) ;
#1537=FACE_OUTER_BOUND ( 'NONE', #18276, .T. ) ;
#1543=PRODUCT_DEFINITION ( 'UNKNOWN', '', #10800, #17216 ) ;
#1547=ORIENTED_EDGE ( 'NONE', *, *, #11386, .T. ) ;
#1551=DIRECTION ( 'NONE',  ( 0.000000000000000000, -1.000000000000000000, 0.000000000000000000 ) ) ;
#1559=EDGE_CURVE ( 'NONE', #15687, #2365, #4194, .T. ) ;
#1595=( NAMED_UNIT ( * ) SI_UNIT ( $, .STERADIAN. ) SOLID_ANGLE_UNIT ( ) );
#1604=FACE_BOUND ( 'NONE', #5895, .T. ) ;
#1623=ADVANCED_FACE ( 'NONE', ( #6315, #6500 ), #17936, .F. ) ;
#1676=ORIENTED_EDGE ( 'NONE', *, *, #10639, .F. ) ;
#1768=CARTESIAN_POINT ( 'NONE',  ( -12.69999999999999929, 3.306546357697854128E-15, 27.00000000000000355 ) ) ;
#1782=( NAMED_UNIT ( * ) SI_UNIT ( $, .STERADIAN. ) SOLID_ANGLE_UNIT ( ) );
#1797=DIRECTION ( 'NONE',  ( 0.000000000000000000, 0.000000000000000000, -1.000000000000000000 ) ) ;
#1806=LINE ( 'NONE', #8848, #5151 ) ;
#1840=CARTESIAN_POINT ( 'NONE',  ( 11.24999999999999645, 0.000000000000000000, 0.000000000000000000 ) ) ;
#1842=DIRECTION ( 'NONE',  ( -1.000000000000000000, -0.000000000000000000, -0.000000000000000000 ) ) ;
#1880=VERTEX_POINT ( 'NONE', #17274 ) ;
#1932=CARTESIAN_POINT ( 'NONE',  ( -12.50000000000000533, 0.000000000000000000, 0.000000000000000000 ) ) ;
#2031=DIRECTION ( 'NONE',  ( -1.000000000000000000, 0.000000000000000000, -0.000000000000000000 ) ) ;
#2106=DIRECTION ( 'NONE',  ( 0.000000000000000000, -1.224646799147330774E-16, 1.000000000000000000 ) ) ;
#2117=ORIENTED_EDGE ( 'NONE', *, *, #5553, .F. ) ;
#2165=DIRECTION ( 'NONE',  ( 0.000000000000000000, 0.000000000000000000, 1.000000000000000000 ) ) ;
#2171=DIRECTION ( 'NONE',  ( 0.000000000000000000, 0.000000000000000000, 1.000000000000000000 ) ) ;
#2181=LINE ( 'NONE', #16853, #17909 ) ;
#2221=EDGE_LOOP ( 'NONE', ( #14978, #848, #7614, #14276 ) ) ;
#2280=DIRECTION ( 'NONE',  ( -1.000000000000000000, -0.000000000000000000, -0.000000000000000000 ) ) ;
#2286=AXIS2_PLACEMENT_3D ( 'NONE', #511, #4890, #905 ) ;
#2348=EDGE_CURVE ( 'NONE', #912, #13113, #1179, .T. ) ;
#2350=CARTESIAN_POINT ( 'NONE',  ( -11.15000000000000391, 0.000000000000000000, 29.90000000000000213 ) ) ;
#2365=VERTEX_POINT ( 'NONE', #15722 ) ;
#2371=AXIS2_PLACEMENT_3D ( 'NONE', #13985, #17044, #2171 ) ;
#2385=AXIS2_PLACEMENT_3D ( 'NONE', #12802, #1551, #7265 ) ;
#2409=DIRECTION ( 'NONE',  ( -1.000000000000000000, -0.000000000000000000, -0.000000000000000000 ) ) ;
#2428=AXIS2_PLACEMENT_3D ( 'NONE', #9490, #9201, #9399 ) ;
#2476=AXIS2_PLACEMENT_3D ( 'NONE', #10047, #7175, #17298 ) ;
#2490=VERTEX_POINT ( 'NONE', #16271 ) ;
#2496=DIRECTION ( 'NONE',  ( 1.000000000000000000, 0.000000000000000000, 0.000000000000000000 ) ) ;
#2553=ORIENTED_EDGE ( 'NONE', *, *, #10792, .F. ) ;
#2567=CARTESIAN_POINT ( 'NONE',  ( -11.25000000000000355, 0.000000000000000000, 0.000000000000000000 ) ) ;
#2680=DIRECTION ( 'NONE',  ( 0.000000000000000000, 0.000000000000000000, -1.000000000000000000 ) ) ;
#2686=AXIS2_PLACEMENT_3D ( 'NONE', #1106, #15379, #3967 ) ;
#2733=TOROIDAL_SURFACE ( 'NONE', #1515, 29.90000000000000213, 0.1000000000000011297 ) ;
#2761=FACE_OUTER_BOUND ( 'NONE', #9221, .T. ) ;
#2775=ORIENTED_EDGE ( 'NONE', *, *, #2348, .T. ) ;
#2782=FACE_OUTER_BOUND ( 'NONE', #15214, .T. ) ;
#2811=CARTESIAN_POINT ( 'NONE',  ( -12.50000000000000355, 0.000000000000000000, -27.00000000000000355 ) ) ;
#2871=ORIENTED_EDGE ( 'NONE', *, *, #18298, .T. ) ;
#2907=CIRCLE ( 'NONE', #17203, 30.00000000000000711 ) ;
#2929=( LENGTH_UNIT ( ) NAMED_UNIT ( * ) SI_UNIT ( .MILLI., .METRE. ) );
#2934=AXIS2_PLACEMENT_3D ( 'NONE', #9482, #13856, #829 ) ;
#2947=ORIENTED_EDGE ( 'NONE', *, *, #10834, .F. ) ;
#2987=DIRECTION ( 'NONE',  ( -1.000000000000000000, -0.000000000000000000, -0.000000000000000000 ) ) ;
#2988=ORIENTED_EDGE ( 'NONE', *, *, #4245, .F. ) ;
#2990=DIRECTION ( 'NONE',  ( 1.000000000000000000, 0.000000000000000000, 0.000000000000000000 ) ) ;
#3000=DIRECTION ( 'NONE',  ( 0.000000000000000000, 0.000000000000000000, 1.000000000000000000 ) ) ;
#3071=ADVANCED_FACE ( 'NONE', ( #12244 ), #13582, .T. ) ;
#3077=ORIENTED_EDGE ( 'NONE', *, *, #15484, .T. ) ;
#3085=EDGE_CURVE ( 'NONE', #7671, #6058, #10831, .T. ) ;
#3104=AXIS2_PLACEMENT_3D ( 'NONE', #12697, #11267, #17089 ) ;
#3127=DIRECTION ( 'NONE',  ( -1.000000000000000000, -0.000000000000000000, -0.000000000000000000 ) ) ;
#3132=DIRECTION ( 'NONE',  ( -1.000000000000000000, -0.000000000000000000, -0.000000000000000000 ) ) ;
#3133=CARTESIAN_POINT ( 'NONE',  ( -12.69999999999999929, 0.000000000000000000, 0.000000000000000000 ) ) ;
#3148=DIRECTION ( 'NONE',  ( 1.000000000000000000, 0.000000000000000000, 0.000000000000000000 ) ) ;
#3151=CARTESIAN_POINT ( 'NONE',  ( -11.15000000000000391, 0.000000000000000000, 0.000000000000000000 ) ) ;
#3154=CARTESIAN_POINT ( 'NONE',  ( -12.69999999999999929, 0.000000000000000000, -28.00000000000000355 ) ) ;
#3158=VERTEX_POINT ( 'NONE', #2811 ) ;
#3163=CARTESIAN_POINT ( 'NONE',  ( 12.49999999999999289, 3.306546357697853733E-15, 27.00000000000000000 ) ) ;
#3187=ORIENTED_EDGE ( 'NONE', *, *, #10546, .F. ) ;
#3208=ORIENTED_EDGE ( 'NONE', *, *, #10834, .T. ) ;
#3243=MANIFOLD_SOLID_BREP ( 'RollersSimplified', #1327 ) ;
#3246=FACE_OUTER_BOUND ( 'NONE', #13686, .T. ) ;
#3330=DIRECTION ( 'NONE',  ( 1.000000000000000000, 0.000000000000000000, 0.000000000000000000 ) ) ;
#3398=CIRCLE ( 'NONE', #16480, 27.00000000000000355 ) ;
#3439=AXIS2_PLACEMENT_3D ( 'NONE', #7520, #17623, #16193 ) ;
#3489=MECHANICAL_DESIGN_GEOMETRIC_PRESENTATION_REPRESENTATION('',(#438),#10171);
#3532=CARTESIAN_POINT ( 'NONE',  ( -12.50000000000000355, 0.000000000000000000, 0.000000000000000000 ) ) ;
#3568=ORIENTED_EDGE ( 'NONE', *, *, #8794, .T. ) ;
#3617=AXIS2_PLACEMENT_3D ( 'NONE', #10139, #9261, #9170 ) ;
#3672=AXIS2_PLACEMENT_3D ( 'NONE', #4965, #3739, #10769 ) ;
#3703=DIRECTION ( 'NONE',  ( -1.000000000000000000, 0.000000000000000000, -0.000000000000000000 ) ) ;
#3725=AXIS2_PLACEMENT_3D ( 'NONE', #13222, #17604, #11795 ) ;
#3739=DIRECTION ( 'NONE',  ( -0.000000000000000000, 1.000000000000000000, 1.224646799147353207E-16 ) ) ;
#3765=ORIENTED_EDGE ( 'NONE', *, *, #7823, .T. ) ;
#3787=ORIENTED_EDGE ( 'NONE', *, *, #5143, .F. ) ;
#3817=VERTEX_POINT ( 'NONE', #3901 ) ;
#3835=CIRCLE ( 'NONE', #5962, 25.00000000000000000 ) ;
#3839=STYLED_ITEM('',(#18876),#3243);
#3856=AXIS2_PLACEMENT_3D ( 'NONE', #3532, #13809, #15332 ) ;
#3860=AXIS2_PLACEMENT_3D ( 'NONE', #4098, #14092, #14296 ) ;
#3888=VERTEX_POINT ( 'NONE', #11406 ) ;
#3901=CARTESIAN_POINT ( 'NONE',  ( -12.50000000000000355, 3.306546357697854128E-15, 27.00000000000000355 ) ) ;
#3942=CARTESIAN_POINT ( 'NONE',  ( -11.15000000000000391, 0.000000000000000000, 0.000000000000000000 ) ) ;
#3947=DIRECTION ( 'NONE',  ( 0.000000000000000000, 0.000000000000000000, 1.000000000000000000 ) ) ;
#3967=DIRECTION ( 'NONE',  ( 0.000000000000000000, 0.000000000000000000, 1.000000000000000000 ) ) ;
#4017=FACE_OUTER_BOUND ( 'NONE', #15667, .T. ) ;
#4020=VECTOR ( 'NONE', #6754, 1000.000000000000000 ) ;
#4066=CARTESIAN_POINT ( 'NONE',  ( -17.77999999999999758, 3.673940397442059967E-15, -30.00000000000000711 ) ) ;
#4098=CARTESIAN_POINT ( 'NONE',  ( 11.25000000000000000, 0.000000000000000000, 0.000000000000000000 ) ) ;
#4115=DIRECTION ( 'NONE',  ( 0.000000000000000000, 0.000000000000000000, -1.000000000000000000 ) ) ;
#4147=DIRECTION ( 'NONE',  ( 0.000000000000000000, 0.000000000000000000, -1.000000000000000000 ) ) ;
#4192=CYLINDRICAL_SURFACE ( 'NONE', #374, 25.00000000000000000 ) ;
#4194=CIRCLE ( 'NONE', #6619, 25.10000000000000142 ) ;
#4234=PRODUCT_CONTEXT ( 'NONE', #16684, 'mechanical' ) ;
#4245=EDGE_CURVE ( 'NONE', #7186, #7123, #16903, .T. ) ;
#4266=EDGE_CURVE ( 'NONE', #912, #11392, #14623, .T. ) ;
#4331=DIRECTION ( 'NONE',  ( 0.000000000000000000, 0.000000000000000000, 1.000000000000000000 ) ) ;
#4418=EDGE_CURVE ( 'NONE', #17588, #432, #3835, .T. ) ;
#4420=( NAMED_UNIT ( * ) PLANE_ANGLE_UNIT ( ) SI_UNIT ( $, .RADIAN. ) );
#4449=SHAPE_REPRESENTATION_RELATIONSHIP ( 'NONE' , 'NONE' ,  #11521, #574 ) ;
#4453=AXIS2_PLACEMENT_3D ( 'NONE', #18592, #8583, #4115 ) ;
#4499=VERTEX_POINT ( 'NONE', #14709 ) ;
#4507=SHAPE_DEFINITION_REPRESENTATION ( #5861, #11521 ) ;
#4510=AXIS2_PLACEMENT_3D ( 'NONE', #14298, #10096, #13230 ) ;
#4556=CARTESIAN_POINT ( 'NONE',  ( -11.25000000000000355, 0.000000000000000000, 0.000000000000000000 ) ) ;
#4638=PRESENTATION_STYLE_ASSIGNMENT (( #15973 ) ) ;
#4646=DIRECTION ( 'NONE',  ( 0.000000000000000000, 0.000000000000000000, -1.000000000000000000 ) ) ;
#4706=CARTESIAN_POINT ( 'NONE',  ( 11.25000000000000000, 3.667817163446322894E-15, -29.90000000000000213 ) ) ;
#4712=ORIENTED_EDGE ( 'NONE', *, *, #16738, .T. ) ;
#4777=ORIENTED_EDGE ( 'NONE', *, *, #13457, .F. ) ;
#4791=CARTESIAN_POINT ( 'NONE',  ( 11.14999999999999680, 0.000000000000000000, 0.000000000000000000 ) ) ;
#4816=TOROIDAL_SURFACE ( 'NONE', #2686, 29.90000000000000213, 0.1000000000000011297 ) ;
#4837=AXIS2_PLACEMENT_3D ( 'NONE', #18708, #11579, #4331 ) ;
#4888=CARTESIAN_POINT ( 'NONE',  ( 11.25000000000000000, 29.90000000000000213, 0.000000000000000000 ) ) ;
#4890=DIRECTION ( 'NONE',  ( -1.000000000000000000, -0.000000000000000000, -0.000000000000000000 ) ) ;
#4943=DIRECTION ( 'NONE',  ( 0.000000000000000000, 0.000000000000000000, 1.000000000000000000 ) ) ;
#4946=ORIENTED_EDGE ( 'NONE', *, *, #10792, .T. ) ;
#4952=CARTESIAN_POINT ( 'NONE',  ( -17.77999999999999758, 0.000000000000000000, 0.000000000000000000 ) ) ;
#4965=CARTESIAN_POINT ( 'NONE',  ( -11.15000000000000391, 3.073863465859856794E-15, -25.10000000000000142 ) ) ;
#5006=AXIS2_PLACEMENT_3D ( 'NONE', #18348, #11103, #5205 ) ;
#5029=ADVANCED_FACE ( 'NONE', ( #1604, #6368 ), #9209, .F. ) ;
#5070=TOROIDAL_SURFACE ( 'NONE', #9023, 25.10000000000000142, 0.09999999999999766020 ) ;
#5127=ORIENTED_EDGE ( 'NONE', *, *, #4245, .T. ) ;
#5143=EDGE_CURVE ( 'NONE', #6058, #7671, #527, .T. ) ;
#5151=VECTOR ( 'NONE', #10186, 1000.000000000000000 ) ;
#5154=EDGE_CURVE ( 'NONE', #7186, #11633, #7683, .T. ) ;
#5184=AXIS2_PLACEMENT_3D ( 'NONE', #12717, #1377, #12614 ) ;
#5185=CIRCLE ( 'NONE', #3672, 0.09999999999999939493 ) ;
#5205=DIRECTION ( 'NONE',  ( 0.000000000000000000, 0.000000000000000000, -1.000000000000000000 ) ) ;
#5229=ORIENTED_EDGE ( 'NONE', *, *, #16930, .T. ) ;
#5257=DIRECTION ( 'NONE',  ( 1.000000000000000000, 0.000000000000000000, 0.000000000000000000 ) ) ;
#5261=ORIENTED_EDGE ( 'NONE', *, *, #1559, .T. ) ;
#5309=CYLINDRICAL_SURFACE ( 'NONE', #12236, 30.00000000000000711 ) ;
#5315=CARTESIAN_POINT ( 'NONE',  ( -11.15000000000000391, 0.000000000000000000, 25.00000000000000000 ) ) ;
#5363=LINE ( 'NONE', #8327, #17575 ) ;
#5397=CARTESIAN_POINT ( 'NONE',  ( -11.25000000000000355, 3.306546357697854128E-15, 27.00000000000000355 ) ) ;
#5403=AXIS2_PLACEMENT_3D ( 'NONE', #18355, #14166, #6936 ) ;
#5467=CARTESIAN_POINT ( 'NONE',  ( 11.14999999999999680, 3.067740231864120904E-15, -25.00000000000000711 ) ) ;
#5519=ORIENTED_EDGE ( 'NONE', *, *, #12027, .F. ) ;
#5542=ADVANCED_FACE ( 'NONE', ( #12549 ), #7822, .T. ) ;
#5553=EDGE_CURVE ( 'NONE', #16785, #15687, #6325, .T. ) ;
#5562=PLANE ( 'NONE',  #5890 ) ;
#5575=CIRCLE ( 'NONE', #3439, 25.00000000000000355 ) ;
#5704=ADVANCED_FACE ( 'NONE', ( #77 ), #1228, .T. ) ;
#5705=FILL_AREA_STYLE_COLOUR ( '', #8645 ) ;
#5728=DIRECTION ( 'NONE',  ( 0.000000000000000000, 0.000000000000000000, -1.000000000000000000 ) ) ;
#5765=DIRECTION ( 'NONE',  ( 0.000000000000000000, 0.000000000000000000, 1.000000000000000000 ) ) ;
#5845=DIRECTION ( 'NONE',  ( 0.000000000000000000, 0.000000000000000000, -1.000000000000000000 ) ) ;
#5853=ORIENTED_EDGE ( 'NONE', *, *, #497, .T. ) ;
#5861=PRODUCT_DEFINITION_SHAPE ( 'NONE', 'NONE',  #1543 ) ;
#5878=DIRECTION ( 'NONE',  ( 1.000000000000000000, 0.000000000000000000, 0.000000000000000000 ) ) ;
#5883=SURFACE_STYLE_FILL_AREA ( #8919 ) ;
#5890=AXIS2_PLACEMENT_3D ( 'NONE', #16026, #2990, #8787 ) ;
#5895=EDGE_LOOP ( 'NONE', ( #8114, #3787 ) ) ;
#5922=ADVANCED_FACE ( 'NONE', ( #8340 ), #4816, .T. ) ;
#5962=AXIS2_PLACEMENT_3D ( 'NONE', #6328, #13481, #423 ) ;
#5968=ORIENTED_EDGE ( 'NONE', *, *, #9689, .T. ) ;
#5977=CIRCLE ( 'NONE', #16634, 27.00000000000000355 ) ;
#6000=CARTESIAN_POINT ( 'NONE',  ( 11.14999999999999680, 0.000000000000000000, 0.000000000000000000 ) ) ;
#6058=VERTEX_POINT ( 'NONE', #15945 ) ;
#6079=CYLINDRICAL_SURFACE ( 'NONE', #18392, 28.00000000000000355 ) ;
#6140=EDGE_CURVE ( 'NONE', #560, #11392, #15481, .T. ) ;
#6156=EDGE_CURVE ( 'NONE', #13103, #432, #16691, .T. ) ;
#6159=DIRECTION ( 'NONE',  ( 0.000000000000000000, 0.000000000000000000, 1.000000000000000000 ) ) ;
#6218=DIRECTION ( 'NONE',  ( 0.000000000000000000, 0.000000000000000000, 1.000000000000000000 ) ) ;
#6282=AXIS2_PLACEMENT_3D ( 'NONE', #4952, #2280, #7998 ) ;
#6299=AXIS2_PLACEMENT_3D ( 'NONE', #6000, #17631, #2165 ) ;
#6315=FACE_OUTER_BOUND ( 'NONE', #17992, .T. ) ;
#6325=CIRCLE ( 'NONE', #5403, 0.09999999999999939493 ) ;
#6328=CARTESIAN_POINT ( 'NONE',  ( -11.15000000000000391, 0.000000000000000000, 0.000000000000000000 ) ) ;
#6343=ADVANCED_FACE ( 'NONE', ( #12507, #7840 ), #10880, .F. ) ;
#6368=FACE_OUTER_BOUND ( 'NONE', #12317, .T. ) ;
#6376=CARTESIAN_POINT ( 'NONE',  ( -11.25000000000000355, 0.000000000000000000, 0.000000000000000000 ) ) ;
#6393=CIRCLE ( 'NONE', #17058, 0.09999999999999939493 ) ;
#6469=CARTESIAN_POINT ( 'NONE',  ( 11.24999999999999645, 0.000000000000000000, 0.000000000000000000 ) ) ;
#6496=DIRECTION ( 'NONE',  ( 1.000000000000000000, 0.000000000000000000, 0.000000000000000000 ) ) ;
#6500=FACE_BOUND ( 'NONE', #1449, .T. ) ;
#6555=VERTEX_POINT ( 'NONE', #17280 ) ;
#6558=EDGE_CURVE ( 'NONE', #2490, #432, #7160, .T. ) ;
#6602=CIRCLE ( 'NONE', #17261, 0.1000000000000028644 ) ;
#6619=AXIS2_PLACEMENT_3D ( 'NONE', #1840, #9257, #15079 ) ;
#6660=ORIENTED_EDGE ( 'NONE', *, *, #507, .T. ) ;
#6666=DIRECTION ( 'NONE',  ( 1.000000000000000000, 0.000000000000000000, 0.000000000000000000 ) ) ;
#6672=ORIENTED_EDGE ( 'NONE', *, *, #154, .T. ) ;
#6754=DIRECTION ( 'NONE',  ( 1.000000000000000000, 0.000000000000000000, 0.000000000000000000 ) ) ;
#6831=FACE_OUTER_BOUND ( 'NONE', #10446, .T. ) ;
#6904=ADVANCED_FACE ( 'NONE', ( #4017 ), #2733, .T. ) ;
#6905=UNCERTAINTY_MEASURE_WITH_UNIT (LENGTH_MEASURE( 1.000000000000000082E-05 ), #2929, 'distance_accuracy_value', 'NONE');
#6936=DIRECTION ( 'NONE',  ( 0.000000000000000000, -1.224646799147334718E-16, 1.000000000000000000 ) ) ;
#7021=EDGE_CURVE ( 'NONE', #13113, #560, #1806, .T. ) ;
#7025=DIRECTION ( 'NONE',  ( 1.000000000000000000, 0.000000000000000000, 0.000000000000000000 ) ) ;
#7052=CARTESIAN_POINT ( 'NONE',  ( -11.15000000000000391, 0.000000000000000000, 0.000000000000000000 ) ) ;
#7080=AXIS2_PLACEMENT_3D ( 'NONE', #1932, #16229, #13745 ) ;
#7123=VERTEX_POINT ( 'NONE', #17619 ) ;
#7141=AXIS2_PLACEMENT_3D ( 'NONE', #6376, #7691, #12183 ) ;
#7160=LINE ( 'NONE', #12987, #9400 ) ;
#7174=CARTESIAN_POINT ( 'NONE',  ( 12.49999999999999289, 0.000000000000000000, 0.000000000000000000 ) ) ;
#7175=DIRECTION ( 'NONE',  ( -1.000000000000000000, -0.000000000000000000, -0.000000000000000000 ) ) ;
#7186=VERTEX_POINT ( 'NONE', #8253 ) ;
#7241=FACE_OUTER_BOUND ( 'NONE', #17969, .T. ) ;
#7265=DIRECTION ( 'NONE',  ( 0.000000000000000000, 0.000000000000000000, -1.000000000000000000 ) ) ;
#7280=CARTESIAN_POINT ( 'NONE',  ( 11.25000000000000000, 0.000000000000000000, 0.000000000000000000 ) ) ;
#7355=CIRCLE ( 'NONE', #11322, 25.10000000000000142 ) ;
#7404=FACE_OUTER_BOUND ( 'NONE', #12295, .T. ) ;
#7412=CARTESIAN_POINT ( 'NONE',  ( 12.49999999999999289, 0.000000000000000000, -28.00000000000000711 ) ) ;
#7443=ORIENTED_EDGE ( 'NONE', *, *, #10297, .T. ) ;
#7483=ORIENTED_EDGE ( 'NONE', *, *, #17625, .F. ) ;
#7520=CARTESIAN_POINT ( 'NONE',  ( 11.14999999999999680, 0.000000000000000000, 0.000000000000000000 ) ) ;
#7536=LINE ( 'NONE', #7628, #18425 ) ;
#7566=AXIS2_PLACEMENT_3D ( 'NONE', #14377, #9897, #1250 ) ;
#7580=DIRECTION ( 'NONE',  ( 1.000000000000000000, 0.000000000000000000, 0.000000000000000000 ) ) ;
#7614=ORIENTED_EDGE ( 'NONE', *, *, #6156, .T. ) ;
#7628=CARTESIAN_POINT ( 'NONE',  ( -12.69999999999999929, 3.429011037612589670E-15, 28.00000000000000355 ) ) ;
#7638=EDGE_LOOP ( 'NONE', ( #9546, #16211, #11703, #18435 ) ) ;
#7671=VERTEX_POINT ( 'NONE', #11171 ) ;
#7675=CARTESIAN_POINT ( 'NONE',  ( 11.25000000000000000, 0.000000000000000000, 0.000000000000000000 ) ) ;
#7683=LINE ( 'NONE', #13509, #10565 ) ;
#7691=DIRECTION ( 'NONE',  ( -1.000000000000000000, -0.000000000000000000, -0.000000000000000000 ) ) ;
#7700=DIRECTION ( 'NONE',  ( 0.000000000000000000, -1.224646799147330774E-16, 1.000000000000000000 ) ) ;
#7702=EDGE_CURVE ( 'NONE', #17281, #179, #5363, .T. ) ;
#7785=AXIS2_PLACEMENT_3D ( 'NONE', #3942, #2409, #8501 ) ;
#7808=CARTESIAN_POINT ( 'NONE',  ( -11.25000000000000355, 0.000000000000000000, 0.000000000000000000 ) ) ;
#7814=AXIS2_PLACEMENT_3D ( 'NONE', #10929, #3703, #14277 ) ;
#7821=ORIENTED_EDGE ( 'NONE', *, *, #13156, .T. ) ;
#7822=TOROIDAL_SURFACE ( 'NONE', #2371, 29.90000000000000213, 0.1000000000000028644 ) ;
#7823=EDGE_CURVE ( 'NONE', #11271, #13113, #16384, .T. ) ;
#7840=FACE_OUTER_BOUND ( 'NONE', #14199, .T. ) ;
#7883=ORIENTED_EDGE ( 'NONE', *, *, #16129, .F. ) ;
#7912=ORIENTED_EDGE ( 'NONE', *, *, #11214, .T. ) ;
#7917=VERTEX_POINT ( 'NONE', #3163 ) ;
#7920=ORIENTED_EDGE ( 'NONE', *, *, #10297, .F. ) ;
#7971=DIRECTION ( 'NONE',  ( 0.000000000000000000, 0.000000000000000000, 1.000000000000000000 ) ) ;
#7992=AXIS2_PLACEMENT_3D ( 'NONE', #15384, #8155, #13967 ) ;
#7998=DIRECTION ( 'NONE',  ( 0.000000000000000000, 0.000000000000000000, 1.000000000000000000 ) ) ;
#8017=AXIS2_PLACEMENT_3D ( 'NONE', #12801, #14324, #9934 ) ;
#8114=ORIENTED_EDGE ( 'NONE', *, *, #3085, .F. ) ;
#8127=AXIS2_PLACEMENT_3D ( 'NONE', #12351, #15505, #654 ) ;
#8134=ORIENTED_EDGE ( 'NONE', *, *, #7702, .T. ) ;
#8139=AXIS2_PLACEMENT_3D ( 'NONE', #4556, #3132, #14940 ) ;
#8155=DIRECTION ( 'NONE',  ( 1.000000000000000000, 0.000000000000000000, 0.000000000000000000 ) ) ;
#8187=DIRECTION ( 'NONE',  ( -1.000000000000000000, -0.000000000000000000, -0.000000000000000000 ) ) ;
#8188=LINE ( 'NONE', #13998, #4020 ) ;
#8223=CARTESIAN_POINT ( 'NONE',  ( 12.49999999999999289, 0.000000000000000000, 0.000000000000000000 ) ) ;
#8253=CARTESIAN_POINT ( 'NONE',  ( 11.25000000000000000, 0.000000000000000000, -28.00000000000000355 ) ) ;
#8264=CYLINDRICAL_SURFACE ( 'NONE', #18413, 25.00000000000000000 ) ;
#8315=ADVANCED_FACE ( 'NONE', ( #8393 ), #15826, .F. ) ;
#8327=CARTESIAN_POINT ( 'NONE',  ( -12.69999999999999929, 0.000000000000000000, -27.00000000000000355 ) ) ;
#8333=ORIENTED_EDGE ( 'NONE', *, *, #7021, .F. ) ;
#8340=FACE_OUTER_BOUND ( 'NONE', #7638, .T. ) ;
#8373=CIRCLE ( 'NONE', #5006, 27.00000000000000000 ) ;
#8393=FACE_OUTER_BOUND ( 'NONE', #10007, .T. ) ;
#8415=ORIENTED_EDGE ( 'NONE', *, *, #6140, .T. ) ;
#8461=FACE_BOUND ( 'NONE', #11970, .T. ) ;
#8462=ORIENTED_EDGE ( 'NONE', *, *, #1559, .F. ) ;
#8501=DIRECTION ( 'NONE',  ( 0.000000000000000000, 0.000000000000000000, 1.000000000000000000 ) ) ;
#8562=EDGE_CURVE ( 'NONE', #16785, #17588, #2181, .T. ) ;
#8579=CARTESIAN_POINT ( 'NONE',  ( 12.49999999999999289, 0.000000000000000000, -27.00000000000000000 ) ) ;
#8583=DIRECTION ( 'NONE',  ( 1.000000000000000000, 0.000000000000000000, 0.000000000000000000 ) ) ;
#8605=AXIS2_PLACEMENT_3D ( 'NONE', #16005, #3148, #5728 ) ;
#8610=EDGE_CURVE ( 'NONE', #2365, #15687, #17333, .T. ) ;
#8645=COLOUR_RGB ( '',1.000000000000000000, 0.9490196078431372140, 0.9098039215686274384 ) ;
#8665=ORIENTED_EDGE ( 'NONE', *, *, #18298, .F. ) ;
#8678=TOROIDAL_SURFACE ( 'NONE', #2286, 29.90000000000000213, 0.1000000000000028644 ) ;
#8730=FACE_OUTER_BOUND ( 'NONE', #8977, .T. ) ;
#8742=PRODUCT ( 'needle roller bearing_nm_iso_ISO 3030 - 15C5060 - 26,SI,AC,26', 'needle roller bearing_nm_iso_ISO 3030 - 15C5060 - 26,SI,AC,26', '', ( #4234 ) ) ;
#8763=AXIS2_PLACEMENT_3D ( 'NONE', #10223, #10325, #5765 ) ;
#8787=DIRECTION ( 'NONE',  ( 0.000000000000000000, 0.000000000000000000, -1.000000000000000000 ) ) ;
#8794=EDGE_CURVE ( 'NONE', #11271, #652, #12759, .T. ) ;
#8817=ORIENTED_EDGE ( 'NONE', *, *, #4266, .F. ) ;
#8832=( LENGTH_UNIT ( ) NAMED_UNIT ( * ) SI_UNIT ( .MILLI., .METRE. ) );
#8848=CARTESIAN_POINT ( 'NONE',  ( -17.77999999999999758, 0.000000000000000000, 30.00000000000000711 ) ) ;
#8915=CARTESIAN_POINT ( 'NONE',  ( -12.69999999999999929, 0.000000000000000000, 0.000000000000000000 ) ) ;
#8919=FILL_AREA_STYLE ('',( #5705 ) ) ;
#8933=CARTESIAN_POINT ( 'NONE',  ( 11.25000000000000000, 0.000000000000000000, 0.000000000000000000 ) ) ;
#8944=ADVANCED_FACE ( 'NONE', ( #10915 ), #12250, .F. ) ;
#8977=EDGE_LOOP ( 'NONE', ( #5127, #5229, #13285, #14991 ) ) ;
#9023=AXIS2_PLACEMENT_3D ( 'NONE', #3151, #13783, #9402 ) ;
#9031=CARTESIAN_POINT ( 'NONE',  ( -11.15000000000000391, 3.061616997868383043E-15, -25.00000000000000000 ) ) ;
#9083=DIRECTION ( 'NONE',  ( 1.000000000000000000, 0.000000000000000000, 0.000000000000000000 ) ) ;
#9110=ORIENTED_EDGE ( 'NONE', *, *, #14480, .F. ) ;
#9115=ORIENTED_EDGE ( 'NONE', *, *, #154, .F. ) ;
#9138=VERTEX_POINT ( 'NONE', #5397 ) ;
#9140=CARTESIAN_POINT ( 'NONE',  ( 11.14999999999999680, 3.661693929450586610E-15, -29.90000000000000213 ) ) ;
#9170=DIRECTION ( 'NONE',  ( 0.000000000000000000, 0.000000000000000000, -1.000000000000000000 ) ) ;
#9176=EDGE_LOOP ( 'NONE', ( #6672, #15778, #1089, #2947 ) ) ;
#9201=DIRECTION ( 'NONE',  ( 1.000000000000000000, 0.000000000000000000, 0.000000000000000000 ) ) ;
#9209=PLANE ( 'NONE',  #11767 ) ;
#9217=CARTESIAN_POINT ( 'NONE',  ( 11.14999999999999680, 0.000000000000000000, 30.00000000000000711 ) ) ;
#9221=EDGE_LOOP ( 'NONE', ( #16195, #9115, #18508, #238 ) ) ;
#9257=DIRECTION ( 'NONE',  ( -1.000000000000000000, -0.000000000000000000, -0.000000000000000000 ) ) ;
#9261=DIRECTION ( 'NONE',  ( 0.000000000000000000, -1.000000000000000000, 0.000000000000000000 ) ) ;
#9299=EDGE_LOOP ( 'NONE', ( #14363, #16893, #14652, #12217 ) ) ;
#9316=DIRECTION ( 'NONE',  ( -1.000000000000000000, -0.000000000000000000, -0.000000000000000000 ) ) ;
#9331=CARTESIAN_POINT ( 'NONE',  ( -11.15000000000000391, 3.661693929450586610E-15, -29.90000000000000213 ) ) ;
#9399=DIRECTION ( 'NONE',  ( 0.000000000000000000, 0.000000000000000000, -1.000000000000000000 ) ) ;
#9400=VECTOR ( 'NONE', #2987, 1000.000000000000000 ) ;
#9402=DIRECTION ( 'NONE',  ( 0.000000000000000000, 0.000000000000000000, 1.000000000000000000 ) ) ;
#9455=DIRECTION ( 'NONE',  ( -1.000000000000000000, 0.000000000000000000, -0.000000000000000000 ) ) ;
#9481=CIRCLE ( 'NONE', #3104, 29.90000000000000213 ) ;
#9482=CARTESIAN_POINT ( 'NONE',  ( -11.25000000000000355, 0.000000000000000000, 0.000000000000000000 ) ) ;
#9486=ORIENTED_EDGE ( 'NONE', *, *, #15721, .T. ) ;
#9490=CARTESIAN_POINT ( 'NONE',  ( -12.69999999999999929, 0.000000000000000000, 0.000000000000000000 ) ) ;
#9501=ORIENTED_EDGE ( 'NONE', *, *, #16738, .F. ) ;
#9546=ORIENTED_EDGE ( 'NONE', *, *, #12793, .F. ) ;
#9549=EDGE_LOOP ( 'NONE', ( #3568, #15386, #5519, #15136 ) ) ;
#9608=ORIENTED_EDGE ( 'NONE', *, *, #1170, .T. ) ;
#9609=VECTOR ( 'NONE', #11828, 1000.000000000000000 ) ;
#9615=CIRCLE ( 'NONE', #7141, 25.10000000000000142 ) ;
#9632=CIRCLE ( 'NONE', #3860, 28.00000000000000355 ) ;
#9669=DIRECTION ( 'NONE',  ( 0.000000000000000000, 0.000000000000000000, 1.000000000000000000 ) ) ;
#9672=CIRCLE ( 'NONE', #244, 28.00000000000000711 ) ;
#9689=EDGE_CURVE ( 'NONE', #15464, #17588, #5185, .T. ) ;
#9699=FACE_OUTER_BOUND ( 'NONE', #10335, .T. ) ;
#9765=UNCERTAINTY_MEASURE_WITH_UNIT (LENGTH_MEASURE( 1.000000000000000082E-05 ), #8832, 'distance_accuracy_value', 'NONE');
#9774=ORIENTED_EDGE ( 'NONE', *, *, #274, .F. ) ;
#9866=ORIENTED_EDGE ( 'NONE', *, *, #8794, .F. ) ;
#9897=DIRECTION ( 'NONE',  ( -1.000000000000000000, -0.000000000000000000, -0.000000000000000000 ) ) ;
#9909=CARTESIAN_POINT ( 'NONE',  ( -12.69999999999999929, 0.000000000000000000, 0.000000000000000000 ) ) ;
#9911=EDGE_LOOP ( 'NONE', ( #15492, #14313 ) ) ;
#9914=AXIS2_PLACEMENT_3D ( 'NONE', #9331, #15160, #2106 ) ;
#9934=DIRECTION ( 'NONE',  ( 1.000000000000000000, 0.000000000000000000, 0.000000000000000000 ) ) ;
#9974=EDGE_LOOP ( 'NONE', ( #2988, #17133 ) ) ;
#9975=AXIS2_PLACEMENT_3D ( 'NONE', #4888, #2031, #10687 ) ;
#10007=EDGE_LOOP ( 'NONE', ( #12435, #13843, #5853, #11958 ) ) ;
#10047=CARTESIAN_POINT ( 'NONE',  ( -11.25000000000000533, 0.000000000000000000, 0.000000000000000000 ) ) ;
#10096=DIRECTION ( 'NONE',  ( -1.000000000000000000, -0.000000000000000000, -0.000000000000000000 ) ) ;
#10102=VECTOR ( 'NONE', #5257, 1000.000000000000000 ) ;
#10139=CARTESIAN_POINT ( 'NONE',  ( -11.15000000000000391, 0.000000000000000000, 25.10000000000000142 ) ) ;
#10171=( GEOMETRIC_REPRESENTATION_CONTEXT ( 3 ) GLOBAL_UNCERTAINTY_ASSIGNED_CONTEXT ( ( #6905 ) ) GLOBAL_UNIT_ASSIGNED_CONTEXT ( ( #2929, #1511, #1782 ) ) REPRESENTATION_CONTEXT ( 'NONE', 'WORKASPACE' ) );
#10186=DIRECTION ( 'NONE',  ( -1.000000000000000000, -0.000000000000000000, -0.000000000000000000 ) ) ;
#10197=PLANE ( 'NONE',  #4453 ) ;
#10223=CARTESIAN_POINT ( 'NONE',  ( -11.25000000000000533, 0.000000000000000000, 0.000000000000000000 ) ) ;
#10297=EDGE_CURVE ( 'NONE', #3888, #7917, #433, .T. ) ;
#10319=AXIS2_PLACEMENT_3D ( 'NONE', #6469, #9316, #4943 ) ;
#10325=DIRECTION ( 'NONE',  ( -1.000000000000000000, -0.000000000000000000, -0.000000000000000000 ) ) ;
#10335=EDGE_LOOP ( 'NONE', ( #18611, #17533, #15083, #8333 ) ) ;
#10339=EDGE_LOOP ( 'NONE', ( #18150, #11738, #7912, #222 ) ) ;
#10367=DIRECTION ( 'NONE',  ( 1.000000000000000000, 0.000000000000000000, 0.000000000000000000 ) ) ;
#10417=AXIS2_PLACEMENT_3D ( 'NONE', #8915, #5878, #1320 ) ;
#10446=EDGE_LOOP ( 'NONE', ( #11875, #1676 ) ) ;
#10483=ORIENTED_EDGE ( 'NONE', *, *, #15399, .T. ) ;
#10504=FACE_OUTER_BOUND ( 'NONE', #9299, .T. ) ;
#10546=EDGE_CURVE ( 'NONE', #1880, #192, #15564, .T. ) ;
#10552=CIRCLE ( 'NONE', #8127, 27.00000000000000355 ) ;
#10565=VECTOR ( 'NONE', #453, 1000.000000000000000 ) ;
#10602=CARTESIAN_POINT ( 'NONE',  ( 11.14999999999999680, 0.000000000000000000, 0.000000000000000000 ) ) ;
#10608=DIRECTION ( 'NONE',  ( 0.000000000000000000, 0.000000000000000000, -1.000000000000000000 ) ) ;
#10639=EDGE_CURVE ( 'NONE', #1486, #4499, #13403, .T. ) ;
#10687=DIRECTION ( 'NONE',  ( -0.000000000000000000, 0.000000000000000000, 1.000000000000000000 ) ) ;
#10769=DIRECTION ( 'NONE',  ( 0.000000000000000000, -1.224646799147334718E-16, 1.000000000000000000 ) ) ;
#10792=EDGE_CURVE ( 'NONE', #17281, #3888, #1533, .T. ) ;
#10800=PRODUCT_DEFINITION_FORMATION_WITH_SPECIFIED_SOURCE ( 'ANY', '', #8742, .NOT_KNOWN. ) ;
#10831=CIRCLE ( 'NONE', #2934, 28.00000000000000355 ) ;
#10834=EDGE_CURVE ( 'NONE', #2490, #2365, #6393, .T. ) ;
#10839=CIRCLE ( 'NONE', #3856, 27.00000000000000355 ) ;
#10863=ORIENTED_EDGE ( 'NONE', *, *, #11386, .F. ) ;
#10880=PLANE ( 'NONE',  #13643 ) ;
#10904=CIRCLE ( 'NONE', #7566, 25.00000000000000000 ) ;
#10909=CARTESIAN_POINT ( 'NONE',  ( 11.14999999999999680, 0.000000000000000000, 0.000000000000000000 ) ) ;
#10915=FACE_OUTER_BOUND ( 'NONE', #1256, .T. ) ;
#10929=CARTESIAN_POINT ( 'NONE',  ( -12.50000000000000355, 28.00000000000000355, 0.000000000000000000 ) ) ;
#10974=ORIENTED_EDGE ( 'NONE', *, *, #11423, .F. ) ;
#11001=DIRECTION ( 'NONE',  ( 1.000000000000000000, 0.000000000000000000, 0.000000000000000000 ) ) ;
#11018=EDGE_CURVE ( 'NONE', #11392, #560, #200, .T. ) ;
#11028=CIRCLE ( 'NONE', #7080, 28.00000000000000355 ) ;
#11037=AXIS2_PLACEMENT_3D ( 'NONE', #9140, #12367, #7700 ) ;
#11103=DIRECTION ( 'NONE',  ( 1.000000000000000000, 0.000000000000000000, 0.000000000000000000 ) ) ;
#11171=CARTESIAN_POINT ( 'NONE',  ( -11.25000000000000355, 0.000000000000000000, -28.00000000000000355 ) ) ;
#11214=EDGE_CURVE ( 'NONE', #4499, #7671, #16292, .T. ) ;
#11232=DIRECTION ( 'NONE',  ( 0.000000000000000000, 0.000000000000000000, -1.000000000000000000 ) ) ;
#11267=DIRECTION ( 'NONE',  ( -1.000000000000000000, -0.000000000000000000, -0.000000000000000000 ) ) ;
#11271=VERTEX_POINT ( 'NONE', #16204 ) ;
#11322=AXIS2_PLACEMENT_3D ( 'NONE', #2567, #17250, #12774 ) ;
#11386=EDGE_CURVE ( 'NONE', #1316, #9138, #5977, .T. ) ;
#11392=VERTEX_POINT ( 'NONE', #388 ) ;
#11406=CARTESIAN_POINT ( 'NONE',  ( 11.25000000000000000, 3.306546357697854128E-15, 27.00000000000000355 ) ) ;
#11411=ADVANCED_FACE ( 'NONE', ( #16674 ), #18001, .T. ) ;
#11415=CARTESIAN_POINT ( 'NONE',  ( 11.25000000000000000, 0.000000000000000000, -27.00000000000000355 ) ) ;
#11418=ORIENTED_EDGE ( 'NONE', *, *, #11423, .T. ) ;
#11423=EDGE_CURVE ( 'NONE', #3158, #3817, #10839, .T. ) ;
#11455=DIRECTION ( 'NONE',  ( -1.000000000000000000, -0.000000000000000000, -0.000000000000000000 ) ) ;
#11506=CARTESIAN_POINT ( 'NONE',  ( -12.69999999999999929, 0.000000000000000000, 0.000000000000000000 ) ) ;
#11521=SHAPE_REPRESENTATION ( 'needle roller bearing_nm_iso_ISO 3030 - 15C5060 - 26,SI,AC,26', ( #8017 ), #16563 ) ;
#11522=CIRCLE ( 'NONE', #16081, 28.00000000000000711 ) ;
#11579=DIRECTION ( 'NONE',  ( -1.000000000000000000, -0.000000000000000000, -0.000000000000000000 ) ) ;
#11628=ORIENTED_EDGE ( 'NONE', *, *, #16911, .F. ) ;
#11633=VERTEX_POINT ( 'NONE', #7412 ) ;
#11635=CARTESIAN_POINT ( 'NONE',  ( -12.69999999999999929, 3.306546357697854128E-15, 27.00000000000000355 ) ) ;
#11703=ORIENTED_EDGE ( 'NONE', *, *, #14864, .T. ) ;
#11738=ORIENTED_EDGE ( 'NONE', *, *, #10639, .T. ) ;
#11767=AXIS2_PLACEMENT_3D ( 'NONE', #17980, #3330, #4646 ) ;
#11795=DIRECTION ( 'NONE',  ( 0.000000000000000000, 0.000000000000000000, -1.000000000000000000 ) ) ;
#11828=DIRECTION ( 'NONE',  ( 1.000000000000000000, 0.000000000000000000, 0.000000000000000000 ) ) ;
#11832=ORIENTED_EDGE ( 'NONE', *, *, #497, .F. ) ;
#11875=ORIENTED_EDGE ( 'NONE', *, *, #16775, .F. ) ;
#11881=EDGE_LOOP ( 'NONE', ( #8817, #2775, #16581, #14977 ) ) ;
#11889=DIRECTION ( 'NONE',  ( -1.000000000000000000, -0.000000000000000000, -0.000000000000000000 ) ) ;
#11958=ORIENTED_EDGE ( 'NONE', *, *, #507, .F. ) ;
#11966=ADVANCED_FACE ( 'NONE', ( #8461, #6831 ), #18642, .T. ) ;
#11970=EDGE_LOOP ( 'NONE', ( #11418, #13128 ) ) ;
#12027=EDGE_CURVE ( 'NONE', #13113, #912, #2907, .T. ) ;
#12111=AXIS2_PLACEMENT_3D ( 'NONE', #9909, #15728, #2680 ) ;
#12183=DIRECTION ( 'NONE',  ( 0.000000000000000000, 0.000000000000000000, 1.000000000000000000 ) ) ;
#12217=ORIENTED_EDGE ( 'NONE', *, *, #11214, .F. ) ;
#12220=ADVANCED_FACE ( 'NONE', ( #15082 ), #8678, .T. ) ;
#12222=CYLINDRICAL_SURFACE ( 'NONE', #18042, 28.00000000000000355 ) ;
#12236=AXIS2_PLACEMENT_3D ( 'NONE', #857, #15512, #12466 ) ;
#12244=FACE_OUTER_BOUND ( 'NONE', #9176, .T. ) ;
#12250=CYLINDRICAL_SURFACE ( 'NONE', #2428, 27.00000000000000355 ) ;
#12260=ORIENTED_EDGE ( 'NONE', *, *, #5154, .T. ) ;
#12295=EDGE_LOOP ( 'NONE', ( #9110, #10974, #6660, #1547 ) ) ;
#12308=ADVANCED_FACE ( 'NONE', ( #14117 ), #14150, .T. ) ;
#12317=EDGE_LOOP ( 'NONE', ( #18474, #10483 ) ) ;
#12346=CARTESIAN_POINT ( 'NONE',  ( -17.77999999999999758, 0.000000000000000000, 0.000000000000000000 ) ) ;
#12351=CARTESIAN_POINT ( 'NONE',  ( -12.50000000000000355, 0.000000000000000000, 0.000000000000000000 ) ) ;
#12367=DIRECTION ( 'NONE',  ( -0.000000000000000000, 1.000000000000000000, 1.224646799147353207E-16 ) ) ;
#12435=ORIENTED_EDGE ( 'NONE', *, *, #1280, .F. ) ;
#12445=CARTESIAN_POINT ( 'NONE',  ( 11.25000000000000000, 0.000000000000000000, 0.000000000000000000 ) ) ;
#12466=DIRECTION ( 'NONE',  ( 0.000000000000000000, 0.000000000000000000, 1.000000000000000000 ) ) ;
#12498=DIRECTION ( 'NONE',  ( 0.000000000000000000, 0.000000000000000000, -1.000000000000000000 ) ) ;
#12502=EDGE_CURVE ( 'NONE', #1486, #6058, #7536, .T. ) ;
#12507=FACE_BOUND ( 'NONE', #9974, .T. ) ;
#12549=FACE_OUTER_BOUND ( 'NONE', #13247, .T. ) ;
#12614=DIRECTION ( 'NONE',  ( 0.000000000000000000, 0.000000000000000000, -1.000000000000000000 ) ) ;
#12621=DIRECTION ( 'NONE',  ( -1.000000000000000000, -0.000000000000000000, -0.000000000000000000 ) ) ;
#12624=ORIENTED_EDGE ( 'NONE', *, *, #8610, .T. ) ;
#12697=CARTESIAN_POINT ( 'NONE',  ( 11.25000000000000000, 0.000000000000000000, 0.000000000000000000 ) ) ;
#12699=CARTESIAN_POINT ( 'NONE',  ( -11.15000000000000391, 0.000000000000000000, 0.000000000000000000 ) ) ;
#12713=CIRCLE ( 'NONE', #8763, 29.90000000000000213 ) ;
#12717=CARTESIAN_POINT ( 'NONE',  ( -12.50000000000000533, 0.000000000000000000, 0.000000000000000000 ) ) ;
#12759=CIRCLE ( 'NONE', #18227, 29.90000000000000213 ) ;
#12774=DIRECTION ( 'NONE',  ( 0.000000000000000000, 0.000000000000000000, 1.000000000000000000 ) ) ;
#12793=EDGE_CURVE ( 'NONE', #11392, #192, #18747, .T. ) ;
#12801=CARTESIAN_POINT ( 'NONE',  ( 0.000000000000000000, 0.000000000000000000, 0.000000000000000000 ) ) ;
#12802=CARTESIAN_POINT ( 'NONE',  ( 11.14999999999999680, 0.000000000000000000, 29.90000000000000213 ) ) ;
#12871=AXIS2_PLACEMENT_3D ( 'NONE', #4791, #414, #13470 ) ;
#12932=EDGE_LOOP ( 'NONE', ( #316, #9608, #12260, #1270 ) ) ;
#12944=DIRECTION ( 'NONE',  ( 0.000000000000000000, 0.000000000000000000, 1.000000000000000000 ) ) ;
#12987=CARTESIAN_POINT ( 'NONE',  ( -17.77999999999999758, 0.000000000000000000, 25.00000000000000000 ) ) ;
#13063=CARTESIAN_POINT ( 'NONE',  ( -11.25000000000000533, 3.667817163446322894E-15, -29.90000000000000213 ) ) ;
#13069=FACE_BOUND ( 'NONE', #1068, .T. ) ;
#13085=FACE_BOUND ( 'NONE', #9911, .T. ) ;
#13103=VERTEX_POINT ( 'NONE', #16658 ) ;
#13113=VERTEX_POINT ( 'NONE', #9217 ) ;
#13127=ORIENTED_EDGE ( 'NONE', *, *, #4418, .T. ) ;
#13128=ORIENTED_EDGE ( 'NONE', *, *, #1280, .T. ) ;
#13130=SURFACE_SIDE_STYLE ('',( #5883 ) ) ;
#13156=EDGE_CURVE ( 'NONE', #13103, #15464, #9615, .T. ) ;
#13184=CARTESIAN_POINT ( 'NONE',  ( -12.50000000000000533, 3.429011037612589670E-15, 28.00000000000000355 ) ) ;
#13222=CARTESIAN_POINT ( 'NONE',  ( -12.69999999999999929, 0.000000000000000000, 0.000000000000000000 ) ) ;
#13230=DIRECTION ( 'NONE',  ( 0.000000000000000000, 0.000000000000000000, 1.000000000000000000 ) ) ;
#13247=EDGE_LOOP ( 'NONE', ( #9774, #1262, #3765, #18385 ) ) ;
#13285=ORIENTED_EDGE ( 'NONE', *, *, #15721, .F. ) ;
#13298=ORIENTED_EDGE ( 'NONE', *, *, #12793, .T. ) ;
#13403=CIRCLE ( 'NONE', #5184, 28.00000000000000355 ) ;
#13412=( NAMED_UNIT ( * ) PLANE_ANGLE_UNIT ( ) SI_UNIT ( $, .RADIAN. ) );
#13457=EDGE_CURVE ( 'NONE', #179, #7917, #8373, .T. ) ;
#13468=CARTESIAN_POINT ( 'NONE',  ( 11.14999999999999680, 0.000000000000000000, 25.10000000000000142 ) ) ;
#13470=DIRECTION ( 'NONE',  ( 0.000000000000000000, 0.000000000000000000, 1.000000000000000000 ) ) ;
#13481=DIRECTION ( 'NONE',  ( -1.000000000000000000, -0.000000000000000000, -0.000000000000000000 ) ) ;
#13509=CARTESIAN_POINT ( 'NONE',  ( -12.69999999999999929, 0.000000000000000000, -28.00000000000000355 ) ) ;
#13540=ADVANCED_FACE ( 'NONE', ( #18258 ), #8264, .F. ) ;
#13582=TOROIDAL_SURFACE ( 'NONE', #493, 25.10000000000000142, 0.09999999999999853451 ) ;
#13631=DIRECTION ( 'NONE',  ( 1.000000000000000000, 0.000000000000000000, 0.000000000000000000 ) ) ;
#13643=AXIS2_PLACEMENT_3D ( 'NONE', #15465, #9455, #18027 ) ;
#13686=EDGE_LOOP ( 'NONE', ( #2117, #4712, #3208, #8462 ) ) ;
#13745=DIRECTION ( 'NONE',  ( 0.000000000000000000, 0.000000000000000000, -1.000000000000000000 ) ) ;
#13783=DIRECTION ( 'NONE',  ( -1.000000000000000000, -0.000000000000000000, -0.000000000000000000 ) ) ;
#13809=DIRECTION ( 'NONE',  ( 1.000000000000000000, 0.000000000000000000, 0.000000000000000000 ) ) ;
#13843=ORIENTED_EDGE ( 'NONE', *, *, #14480, .T. ) ;
#13856=DIRECTION ( 'NONE',  ( -1.000000000000000000, -0.000000000000000000, -0.000000000000000000 ) ) ;
#13927=AXIS2_PLACEMENT_3D ( 'NONE', #11506, #7025, #17322 ) ;
#13967=DIRECTION ( 'NONE',  ( 0.000000000000000000, 0.000000000000000000, -1.000000000000000000 ) ) ;
#13985=CARTESIAN_POINT ( 'NONE',  ( 11.14999999999999680, 0.000000000000000000, 0.000000000000000000 ) ) ;
#13998=CARTESIAN_POINT ( 'NONE',  ( -12.69999999999999929, 0.000000000000000000, -27.00000000000000355 ) ) ;
#14027=CARTESIAN_POINT ( 'NONE',  ( 11.24999999999999645, 3.073863465859856794E-15, -25.10000000000000142 ) ) ;
#14066=DIRECTION ( 'NONE',  ( -1.000000000000000000, -0.000000000000000000, -0.000000000000000000 ) ) ;
#14092=DIRECTION ( 'NONE',  ( 1.000000000000000000, 0.000000000000000000, 0.000000000000000000 ) ) ;
#14117=FACE_OUTER_BOUND ( 'NONE', #2221, .T. ) ;
#14150=TOROIDAL_SURFACE ( 'NONE', #16579, 25.10000000000000142, 0.09999999999999766020 ) ;
#14158=DIRECTION ( 'NONE',  ( 0.000000000000000000, 0.000000000000000000, -1.000000000000000000 ) ) ;
#14166=DIRECTION ( 'NONE',  ( -0.000000000000000000, 1.000000000000000000, 1.224646799147353207E-16 ) ) ;
#14199=EDGE_LOOP ( 'NONE', ( #9866, #11628 ) ) ;
#14200=DIRECTION ( 'NONE',  ( -1.000000000000000000, -0.000000000000000000, -0.000000000000000000 ) ) ;
#14276=ORIENTED_EDGE ( 'NONE', *, *, #4418, .F. ) ;
#14277=DIRECTION ( 'NONE',  ( -0.000000000000000000, 0.000000000000000000, 1.000000000000000000 ) ) ;
#14296=DIRECTION ( 'NONE',  ( 0.000000000000000000, 0.000000000000000000, 1.000000000000000000 ) ) ;
#14298=CARTESIAN_POINT ( 'NONE',  ( 11.14999999999999680, 0.000000000000000000, 0.000000000000000000 ) ) ;
#14313=ORIENTED_EDGE ( 'NONE', *, *, #17503, .F. ) ;
#14324=DIRECTION ( 'NONE',  ( 0.000000000000000000, 0.000000000000000000, 1.000000000000000000 ) ) ;
#14328=CARTESIAN_POINT ( 'NONE',  ( 11.14999999999999680, 3.673940397442059967E-15, -30.00000000000000711 ) ) ;
#14363=ORIENTED_EDGE ( 'NONE', *, *, #16775, .T. ) ;
#14377=CARTESIAN_POINT ( 'NONE',  ( -11.15000000000000391, 0.000000000000000000, 0.000000000000000000 ) ) ;
#14394=CIRCLE ( 'NONE', #7992, 27.00000000000000000 ) ;
#14474=ADVANCED_FACE ( 'NONE', ( #2782, #13069 ), #10197, .T. ) ;
#14478=( GEOMETRIC_REPRESENTATION_CONTEXT ( 3 ) GLOBAL_UNCERTAINTY_ASSIGNED_CONTEXT ( ( #18333 ) ) GLOBAL_UNIT_ASSIGNED_CONTEXT ( ( #17749, #4420, #16143 ) ) REPRESENTATION_CONTEXT ( 'NONE', 'WORKASPACE' ) );
#14480=EDGE_CURVE ( 'NONE', #3817, #9138, #15921, .T. ) ;
#14498=FACE_OUTER_BOUND ( 'NONE', #354, .T. ) ;
#14512=CARTESIAN_POINT ( 'NONE',  ( -11.25000000000000355, 3.073863465859856794E-15, -25.10000000000000142 ) ) ;
#14623=LINE ( 'NONE', #4066, #16597 ) ;
#14649=CYLINDRICAL_SURFACE ( 'NONE', #3725, 27.00000000000000355 ) ;
#14652=ORIENTED_EDGE ( 'NONE', *, *, #5143, .T. ) ;
#14664=CIRCLE ( 'NONE', #17110, 27.00000000000000355 ) ;
#14690=ADVANCED_FACE ( 'NONE', ( #1537 ), #5070, .T. ) ;
#14709=CARTESIAN_POINT ( 'NONE',  ( -12.50000000000000533, 0.000000000000000000, -28.00000000000000355 ) ) ;
#14717=ADVANCED_FACE ( 'NONE', ( #3246 ), #16029, .T. ) ;
#14846=FACE_OUTER_BOUND ( 'NONE', #10339, .T. ) ;
#14864=EDGE_CURVE ( 'NONE', #560, #1880, #6602, .T. ) ;
#14940=DIRECTION ( 'NONE',  ( 0.000000000000000000, 0.000000000000000000, -1.000000000000000000 ) ) ;
#14977=ORIENTED_EDGE ( 'NONE', *, *, #11018, .F. ) ;
#14978=ORIENTED_EDGE ( 'NONE', *, *, #9689, .F. ) ;
#14991=ORIENTED_EDGE ( 'NONE', *, *, #5154, .F. ) ;
#15079=DIRECTION ( 'NONE',  ( 0.000000000000000000, 0.000000000000000000, 1.000000000000000000 ) ) ;
#15082=FACE_OUTER_BOUND ( 'NONE', #9549, .T. ) ;
#15083=ORIENTED_EDGE ( 'NONE', *, *, #6140, .F. ) ;
#15085=MECHANICAL_DESIGN_GEOMETRIC_PRESENTATION_REPRESENTATION('',(#3839),#14478);
#15105=VECTOR ( 'NONE', #2496, 1000.000000000000000 ) ;
#15136=ORIENTED_EDGE ( 'NONE', *, *, #7823, .F. ) ;
#15160=DIRECTION ( 'NONE',  ( -0.000000000000000000, 1.000000000000000000, 1.224646799147353207E-16 ) ) ;
#15214=EDGE_LOOP ( 'NONE', ( #9486, #3077 ) ) ;
#15236=EDGE_LOOP ( 'NONE', ( #9501, #18071, #13127, #18636 ) ) ;
#15247=DIRECTION ( 'NONE',  ( 0.000000000000000000, 0.000000000000000000, -1.000000000000000000 ) ) ;
#15308=DIRECTION ( 'NONE',  ( 0.000000000000000000, -1.000000000000000000, 0.000000000000000000 ) ) ;
#15332=DIRECTION ( 'NONE',  ( 0.000000000000000000, 0.000000000000000000, -1.000000000000000000 ) ) ;
#15379=DIRECTION ( 'NONE',  ( -1.000000000000000000, -0.000000000000000000, -0.000000000000000000 ) ) ;
#15384=CARTESIAN_POINT ( 'NONE',  ( 12.49999999999999289, 0.000000000000000000, 0.000000000000000000 ) ) ;
#15386=ORIENTED_EDGE ( 'NONE', *, *, #274, .T. ) ;
#15399=EDGE_CURVE ( 'NONE', #192, #1880, #12713, .T. ) ;
#15464=VERTEX_POINT ( 'NONE', #14512 ) ;
#15465=CARTESIAN_POINT ( 'NONE',  ( 11.25000000000000000, 29.90000000000000213, 0.000000000000000000 ) ) ;
#15481=CIRCLE ( 'NONE', #4837, 30.00000000000000711 ) ;
#15484=EDGE_CURVE ( 'NONE', #6555, #11633, #9672, .T. ) ;
#15485=ORIENTED_EDGE ( 'NONE', *, *, #6156, .F. ) ;
#15492=ORIENTED_EDGE ( 'NONE', *, *, #13156, .F. ) ;
#15505=DIRECTION ( 'NONE',  ( 1.000000000000000000, 0.000000000000000000, 0.000000000000000000 ) ) ;
#15512=DIRECTION ( 'NONE',  ( -1.000000000000000000, -0.000000000000000000, -0.000000000000000000 ) ) ;
#15564=CIRCLE ( 'NONE', #2476, 29.90000000000000213 ) ;
#15667=EDGE_LOOP ( 'NONE', ( #8415, #13298, #3187, #16888 ) ) ;
#15687=VERTEX_POINT ( 'NONE', #14027 ) ;
#15721=EDGE_CURVE ( 'NONE', #11633, #6555, #11522, .T. ) ;
#15722=CARTESIAN_POINT ( 'NONE',  ( 11.24999999999999645, 0.000000000000000000, 25.10000000000000142 ) ) ;
#15728=DIRECTION ( 'NONE',  ( 1.000000000000000000, 0.000000000000000000, 0.000000000000000000 ) ) ;
#15778=ORIENTED_EDGE ( 'NONE', *, *, #5553, .T. ) ;
#15826=CYLINDRICAL_SURFACE ( 'NONE', #12111, 27.00000000000000355 ) ;
#15921=LINE ( 'NONE', #11635, #15105 ) ;
#15945=CARTESIAN_POINT ( 'NONE',  ( -11.25000000000000355, 3.429011037612589670E-15, 28.00000000000000355 ) ) ;
#15973=SURFACE_STYLE_USAGE ( .BOTH. , #13130 ) ;
#15976=ADVANCED_FACE ( 'NONE', ( #14498, #13085 ), #5562, .F. ) ;
#16005=CARTESIAN_POINT ( 'NONE',  ( -12.69999999999999929, 0.000000000000000000, 0.000000000000000000 ) ) ;
#16026=CARTESIAN_POINT ( 'NONE',  ( -11.25000000000000355, 29.90000000000000213, 0.000000000000000000 ) ) ;
#16029=TOROIDAL_SURFACE ( 'NONE', #6299, 25.10000000000000142, 0.09999999999999853451 ) ;
#16081=AXIS2_PLACEMENT_3D ( 'NONE', #8223, #6496, #12498 ) ;
#16083=CARTESIAN_POINT ( 'NONE',  ( -17.77999999999999758, 0.000000000000000000, 0.000000000000000000 ) ) ;
#16129=EDGE_CURVE ( 'NONE', #432, #17588, #10904, .T. ) ;
#16133=AXIS2_PLACEMENT_3D ( 'NONE', #7280, #16138, #3000 ) ;
#16138=DIRECTION ( 'NONE',  ( -1.000000000000000000, -0.000000000000000000, -0.000000000000000000 ) ) ;
#16143=( NAMED_UNIT ( * ) SI_UNIT ( $, .STERADIAN. ) SOLID_ANGLE_UNIT ( ) );
#16164=CYLINDRICAL_SURFACE ( 'NONE', #10417, 28.00000000000000355 ) ;
#16176=ORIENTED_EDGE ( 'NONE', *, *, #13457, .T. ) ;
#16193=DIRECTION ( 'NONE',  ( 0.000000000000000000, 0.000000000000000000, 1.000000000000000000 ) ) ;
#16195=ORIENTED_EDGE ( 'NONE', *, *, #8562, .F. ) ;
#16200=CIRCLE ( 'NONE', #12871, 25.00000000000000355 ) ;
#16204=CARTESIAN_POINT ( 'NONE',  ( 11.25000000000000000, 0.000000000000000000, 29.90000000000000213 ) ) ;
#16208=DIRECTION ( 'NONE',  ( 1.000000000000000000, 0.000000000000000000, 0.000000000000000000 ) ) ;
#16211=ORIENTED_EDGE ( 'NONE', *, *, #11018, .T. ) ;
#16229=DIRECTION ( 'NONE',  ( 1.000000000000000000, 0.000000000000000000, 0.000000000000000000 ) ) ;
#16271=CARTESIAN_POINT ( 'NONE',  ( 11.14999999999999680, 0.000000000000000000, 25.00000000000000355 ) ) ;
#16285=ADVANCED_FACE ( 'NONE', ( #14846 ), #6079, .T. ) ;
#16292=LINE ( 'NONE', #3154, #9609 ) ;
#16301=AXIS2_PLACEMENT_3D ( 'NONE', #12445, #11001, #17116 ) ;
#16324=CARTESIAN_POINT ( 'NONE',  ( -12.69999999999999929, 0.000000000000000000, 0.000000000000000000 ) ) ;
#16384=CIRCLE ( 'NONE', #2385, 0.1000000000000028644 ) ;
#16474=VECTOR ( 'NONE', #7580, 1000.000000000000000 ) ;
#16480=AXIS2_PLACEMENT_3D ( 'NONE', #863, #6666, #11232 ) ;
#16563=( GEOMETRIC_REPRESENTATION_CONTEXT ( 3 ) GLOBAL_UNCERTAINTY_ASSIGNED_CONTEXT ( ( #9765 ) ) GLOBAL_UNIT_ASSIGNED_CONTEXT ( ( #8832, #13412, #1595 ) ) REPRESENTATION_CONTEXT ( 'NONE', 'WORKASPACE' ) );
#16579=AXIS2_PLACEMENT_3D ( 'NONE', #12699, #11455, #3947 ) ;
#16581=ORIENTED_EDGE ( 'NONE', *, *, #7021, .T. ) ;
#16597=VECTOR ( 'NONE', #18718, 1000.000000000000000 ) ;
#16634=AXIS2_PLACEMENT_3D ( 'NONE', #7808, #13631, #15247 ) ;
#16658=CARTESIAN_POINT ( 'NONE',  ( -11.25000000000000355, 0.000000000000000000, 25.10000000000000142 ) ) ;
#16674=FACE_OUTER_BOUND ( 'NONE', #11881, .T. ) ;
#16684=APPLICATION_CONTEXT ( 'automotive_design' ) ;
#16691=CIRCLE ( 'NONE', #3617, 0.09999999999999939493 ) ;
#16738=EDGE_CURVE ( 'NONE', #16785, #2490, #16200, .T. ) ;
#16775=EDGE_CURVE ( 'NONE', #4499, #1486, #11028, .T. ) ;
#16785=VERTEX_POINT ( 'NONE', #5467 ) ;
#16853=CARTESIAN_POINT ( 'NONE',  ( -17.77999999999999758, 3.061616997868383043E-15, -25.00000000000000000 ) ) ;
#16888=ORIENTED_EDGE ( 'NONE', *, *, #14864, .F. ) ;
#16893=ORIENTED_EDGE ( 'NONE', *, *, #12502, .T. ) ;
#16903=CIRCLE ( 'NONE', #16301, 28.00000000000000355 ) ;
#16911=EDGE_CURVE ( 'NONE', #652, #11271, #9481, .T. ) ;
#16930=EDGE_CURVE ( 'NONE', #7123, #6555, #795, .T. ) ;
#17044=DIRECTION ( 'NONE',  ( -1.000000000000000000, -0.000000000000000000, -0.000000000000000000 ) ) ;
#17058=AXIS2_PLACEMENT_3D ( 'NONE', #13468, #49, #5845 ) ;
#17089=DIRECTION ( 'NONE',  ( 0.000000000000000000, 0.000000000000000000, 1.000000000000000000 ) ) ;
#17110=AXIS2_PLACEMENT_3D ( 'NONE', #8933, #11889, #17347 ) ;
#17116=DIRECTION ( 'NONE',  ( 0.000000000000000000, 0.000000000000000000, 1.000000000000000000 ) ) ;
#17133=ORIENTED_EDGE ( 'NONE', *, *, #1170, .F. ) ;
#17203=AXIS2_PLACEMENT_3D ( 'NONE', #10602, #1842, #6218 ) ;
#17216=PRODUCT_DEFINITION_CONTEXT ( 'detailed design', #18627, 'design' ) ;
#17250=DIRECTION ( 'NONE',  ( -1.000000000000000000, -0.000000000000000000, -0.000000000000000000 ) ) ;
#17261=AXIS2_PLACEMENT_3D ( 'NONE', #2350, #15308, #14158 ) ;
#17274=CARTESIAN_POINT ( 'NONE',  ( -11.25000000000000533, 0.000000000000000000, 29.90000000000000213 ) ) ;
#17280=CARTESIAN_POINT ( 'NONE',  ( 12.49999999999999289, 3.429011037612590065E-15, 28.00000000000001066 ) ) ;
#17281=VERTEX_POINT ( 'NONE', #11415 ) ;
#17295=ADVANCED_FACE ( 'NONE', ( #2761 ), #4192, .F. ) ;
#17298=DIRECTION ( 'NONE',  ( 0.000000000000000000, 0.000000000000000000, 1.000000000000000000 ) ) ;
#17322=DIRECTION ( 'NONE',  ( 0.000000000000000000, 0.000000000000000000, -1.000000000000000000 ) ) ;
#17333=CIRCLE ( 'NONE', #10319, 25.10000000000000142 ) ;
#17345=ADVANCED_FACE ( 'NONE', ( #7404 ), #14649, .F. ) ;
#17347=DIRECTION ( 'NONE',  ( 0.000000000000000000, 0.000000000000000000, 1.000000000000000000 ) ) ;
#17441=CIRCLE ( 'NONE', #11037, 0.1000000000000028644 ) ;
#17503=EDGE_CURVE ( 'NONE', #15464, #13103, #7355, .T. ) ;
#17533=ORIENTED_EDGE ( 'NONE', *, *, #4266, .T. ) ;
#17575=VECTOR ( 'NONE', #18229, 1000.000000000000000 ) ;
#17588=VERTEX_POINT ( 'NONE', #9031 ) ;
#17598=DIRECTION ( 'NONE',  ( -1.000000000000000000, -0.000000000000000000, -0.000000000000000000 ) ) ;
#17604=DIRECTION ( 'NONE',  ( 1.000000000000000000, 0.000000000000000000, 0.000000000000000000 ) ) ;
#17619=CARTESIAN_POINT ( 'NONE',  ( 11.25000000000000000, 3.429011037612589670E-15, 28.00000000000000355 ) ) ;
#17623=DIRECTION ( 'NONE',  ( -1.000000000000000000, -0.000000000000000000, -0.000000000000000000 ) ) ;
#17625=EDGE_CURVE ( 'NONE', #3888, #17281, #14664, .T. ) ;
#17631=DIRECTION ( 'NONE',  ( -1.000000000000000000, -0.000000000000000000, -0.000000000000000000 ) ) ;
#17749=( LENGTH_UNIT ( ) NAMED_UNIT ( * ) SI_UNIT ( .MILLI., .METRE. ) );
#17852=CARTESIAN_POINT ( 'NONE',  ( -11.15000000000000391, 0.000000000000000000, 30.00000000000000711 ) ) ;
#17855=ADVANCED_FACE ( 'NONE', ( #9699 ), #5309, .T. ) ;
#17878=ORIENTED_EDGE ( 'NONE', *, *, #17625, .T. ) ;
#17909=VECTOR ( 'NONE', #8187, 1000.000000000000000 ) ;
#17936=PLANE ( 'NONE',  #9975 ) ;
#17965=ADVANCED_FACE ( 'NONE', ( #8730 ), #16164, .T. ) ;
#17969=EDGE_LOOP ( 'NONE', ( #4946, #7443, #2871, #54 ) ) ;
#17980=CARTESIAN_POINT ( 'NONE',  ( -11.25000000000000355, 29.90000000000000213, 0.000000000000000000 ) ) ;
#17992=EDGE_LOOP ( 'NONE', ( #2553, #7483 ) ) ;
#18001=CYLINDRICAL_SURFACE ( 'NONE', #6282, 30.00000000000000711 ) ;
#18027=DIRECTION ( 'NONE',  ( -0.000000000000000000, 0.000000000000000000, 1.000000000000000000 ) ) ;
#18042=AXIS2_PLACEMENT_3D ( 'NONE', #16324, #9083, #10608 ) ;
#18071=ORIENTED_EDGE ( 'NONE', *, *, #8562, .T. ) ;
#18150=ORIENTED_EDGE ( 'NONE', *, *, #12502, .F. ) ;
#18227=AXIS2_PLACEMENT_3D ( 'NONE', #7675, #17598, #6159 ) ;
#18229=DIRECTION ( 'NONE',  ( 1.000000000000000000, 0.000000000000000000, 0.000000000000000000 ) ) ;
#18258=FACE_OUTER_BOUND ( 'NONE', #15236, .T. ) ;
#18276=EDGE_LOOP ( 'NONE', ( #7821, #5968, #7883, #15485 ) ) ;
#18298=EDGE_CURVE ( 'NONE', #7917, #179, #14394, .T. ) ;
#18309=CARTESIAN_POINT ( 'NONE',  ( -12.69999999999999929, 3.429011037612589670E-15, 28.00000000000000355 ) ) ;
#18333=UNCERTAINTY_MEASURE_WITH_UNIT (LENGTH_MEASURE( 1.000000000000000082E-05 ), #17749, 'distance_accuracy_value', 'NONE');
#18348=CARTESIAN_POINT ( 'NONE',  ( 12.49999999999999289, 0.000000000000000000, 0.000000000000000000 ) ) ;
#18355=CARTESIAN_POINT ( 'NONE',  ( 11.14999999999999680, 3.073863465859856794E-15, -25.10000000000000142 ) ) ;
#18385=ORIENTED_EDGE ( 'NONE', *, *, #2348, .F. ) ;
#18392=AXIS2_PLACEMENT_3D ( 'NONE', #3133, #10367, #1797 ) ;
#18413=AXIS2_PLACEMENT_3D ( 'NONE', #12346, #14066, #7971 ) ;
#18425=VECTOR ( 'NONE', #16208, 1000.000000000000000 ) ;
#18435=ORIENTED_EDGE ( 'NONE', *, *, #15399, .F. ) ;
#18474=ORIENTED_EDGE ( 'NONE', *, *, #10546, .T. ) ;
#18508=ORIENTED_EDGE ( 'NONE', *, *, #6558, .T. ) ;
#18585=ADVANCED_FACE ( 'NONE', ( #10504 ), #12222, .T. ) ;
#18592=CARTESIAN_POINT ( 'NONE',  ( 12.49999999999999289, 27.00000000000000000, 0.000000000000000000 ) ) ;
#18611=ORIENTED_EDGE ( 'NONE', *, *, #12027, .T. ) ;
#18627=APPLICATION_CONTEXT ( 'automotive_design' ) ;
#18636=ORIENTED_EDGE ( 'NONE', *, *, #6558, .F. ) ;
#18642=PLANE ( 'NONE',  #7814 ) ;
#18708=CARTESIAN_POINT ( 'NONE',  ( -11.15000000000000391, 0.000000000000000000, 0.000000000000000000 ) ) ;
#18718=DIRECTION ( 'NONE',  ( -1.000000000000000000, -0.000000000000000000, -0.000000000000000000 ) ) ;
#18747=CIRCLE ( 'NONE', #9914, 0.1000000000000028644 ) ;
#18870=COLOUR_RGB('Grey',0.48,0.52,0.57);
#18871=FILL_AREA_STYLE_COLOUR('',#18870);
#18872=FILL_AREA_STYLE('',(#18871));
#18873=SURFACE_STYLE_FILL_AREA(#18872);
#18874=SURFACE_SIDE_STYLE('',(#18873));
#18875=SURFACE_STYLE_USAGE(.BOTH.,#18874);
#18876=PRESENTATION_STYLE_ASSIGNMENT((#18875));
ENDSEC;
END-ISO-10303-21;
